ISO-10303-21;
HEADER;
/* Generated by software containing ST-Developer
 * from STEP Tools, Inc. (www.steptools.com) 
 */

FILE_DESCRIPTION(
/* description */ ('Hand wheel with handle and shaft collar'),
/* implementation_level */ '2;1');

FILE_NAME(
/* name */ 'Socket Set Screw - M5x8.step',
/* time_stamp */ '2026-10-28T03:23:19-07:00',
/* author */ (''),
/* organization */ (''),
/* preprocessor_version */ 'ST-DEVELOPER v20.2',
/* originating_system */ 'Autodesk Translation Framework v15.17.0.0',
/* authorisation */ '');

FILE_SCHEMA (('AUTOMOTIVE_DESIGN { 1 0 10303 214 3 1 1 }'));
ENDSEC;

DATA;
#10=MECHANICAL_DESIGN_GEOMETRIC_PRESENTATION_REPRESENTATION('',(#424),#10510);
#312=CONICAL_SURFACE('',#6161,0.235,0.785398163397448);
#313=CONICAL_SURFACE('',#6165,0.2125,0.785398163397448);
#353=SHAPE_REPRESENTATION_RELATIONSHIP('SRR','None',#10671,#385);
#385=ADVANCED_BREP_SHAPE_REPRESENTATION('',(#470),#10498);
#424=STYLED_ITEM('',(#10915),#470);
#470=MANIFOLD_SOLID_BREP('Body1',#5324);
#581=FACE_BOUND('',#1398,.T.);
#710=PLANE('',#6152);
#711=PLANE('',#6153);
#712=PLANE('',#6154);
#713=PLANE('',#6155);
#714=PLANE('',#6156);
#715=PLANE('',#6157);
#716=PLANE('',#6158);
#717=PLANE('',#6159);
#718=PLANE('',#6167);
#976=FACE_OUTER_BOUND('',#1390,.T.);
#977=FACE_OUTER_BOUND('',#1391,.T.);
#978=FACE_OUTER_BOUND('',#1392,.T.);
#979=FACE_OUTER_BOUND('',#1393,.T.);
#980=FACE_OUTER_BOUND('',#1394,.T.);
#981=FACE_OUTER_BOUND('',#1395,.T.);
#982=FACE_OUTER_BOUND('',#1396,.T.);
#983=FACE_OUTER_BOUND('',#1397,.T.);
#984=FACE_OUTER_BOUND('',#1399,.T.);
#985=FACE_OUTER_BOUND('',#1400,.T.);
#986=FACE_OUTER_BOUND('',#1401,.T.);
#987=FACE_OUTER_BOUND('',#1402,.T.);
#1390=EDGE_LOOP('',(#4463,#4464,#4465,#4466));
#1391=EDGE_LOOP('',(#4467,#4468,#4469,#4470));
#1392=EDGE_LOOP('',(#4471,#4472,#4473,#4474));
#1393=EDGE_LOOP('',(#4475,#4476,#4477,#4478));
#1394=EDGE_LOOP('',(#4479,#4480,#4481,#4482));
#1395=EDGE_LOOP('',(#4483,#4484,#4485,#4486));
#1396=EDGE_LOOP('',(#4487,#4488,#4489,#4490,#4491,#4492));
#1397=EDGE_LOOP('',(#4493));
#1398=EDGE_LOOP('',(#4494,#4495,#4496,#4497,#4498,#4499));
#1399=EDGE_LOOP('',(#4500,#4501,#4502,#4503));
#1400=EDGE_LOOP('',(#4504,#4505,#4506,#4507));
#1401=EDGE_LOOP('',(#4508,#4509,#4510,#4511));
#1402=EDGE_LOOP('',(#4512));
#1734=LINE('',#9579,#2044);
#1735=LINE('',#9581,#2045);
#1736=LINE('',#9583,#2046);
#1737=LINE('',#9584,#2047);
#1738=LINE('',#9587,#2048);
#1739=LINE('',#9589,#2049);
#1740=LINE('',#9590,#2050);
#1741=LINE('',#9593,#2051);
#1742=LINE('',#9595,#2052);
#1743=LINE('',#9596,#2053);
#1744=LINE('',#9599,#2054);
#1745=LINE('',#9601,#2055);
#1746=LINE('',#9602,#2056);
#1747=LINE('',#9605,#2057);
#1748=LINE('',#9607,#2058);
#1749=LINE('',#9608,#2059);
#1750=LINE('',#9610,#2060);
#1751=LINE('',#9611,#2061);
#1752=LINE('',#9619,#2062);
#1753=LINE('',#9623,#2063);
#1754=LINE('',#9627,#2064);
#2044=VECTOR('',#7552,1.);
#2045=VECTOR('',#7553,1.);
#2046=VECTOR('',#7554,1.);
#2047=VECTOR('',#7555,1.);
#2048=VECTOR('',#7558,1.);
#2049=VECTOR('',#7559,1.);
#2050=VECTOR('',#7560,1.);
#2051=VECTOR('',#7563,1.);
#2052=VECTOR('',#7564,1.);
#2053=VECTOR('',#7565,1.);
#2054=VECTOR('',#7568,1.);
#2055=VECTOR('',#7569,1.);
#2056=VECTOR('',#7570,1.);
#2057=VECTOR('',#7573,1.);
#2058=VECTOR('',#7574,1.);
#2059=VECTOR('',#7575,1.);
#2060=VECTOR('',#7578,1.);
#2061=VECTOR('',#7579,1.);
#2062=VECTOR('',#7590,0.235);
#2063=VECTOR('',#7595,0.25);
#2064=VECTOR('',#7600,0.2125);
#2343=CIRCLE('',#6160,0.22);
#2344=CIRCLE('',#6162,0.24505);
#2345=CIRCLE('',#6164,0.24505);
#2346=CIRCLE('',#6166,0.175);
#2751=VERTEX_POINT('',#9577);
#2752=VERTEX_POINT('',#9578);
#2753=VERTEX_POINT('',#9580);
#2754=VERTEX_POINT('',#9582);
#2755=VERTEX_POINT('',#9586);
#2756=VERTEX_POINT('',#9588);
#2757=VERTEX_POINT('',#9592);
#2758=VERTEX_POINT('',#9594);
#2759=VERTEX_POINT('',#9598);
#2760=VERTEX_POINT('',#9600);
#2761=VERTEX_POINT('',#9604);
#2762=VERTEX_POINT('',#9606);
#2763=VERTEX_POINT('',#9614);
#2764=VERTEX_POINT('',#9617);
#2765=VERTEX_POINT('',#9621);
#2766=VERTEX_POINT('',#9625);
#3349=EDGE_CURVE('',#2751,#2752,#1734,.T.);
#3350=EDGE_CURVE('',#2751,#2753,#1735,.T.);
#3351=EDGE_CURVE('',#2753,#2754,#1736,.T.);
#3352=EDGE_CURVE('',#2752,#2754,#1737,.T.);
#3353=EDGE_CURVE('',#2755,#2751,#1738,.T.);
#3354=EDGE_CURVE('',#2755,#2756,#1739,.T.);
#3355=EDGE_CURVE('',#2756,#2753,#1740,.T.);
#3356=EDGE_CURVE('',#2757,#2755,#1741,.T.);
#3357=EDGE_CURVE('',#2757,#2758,#1742,.T.);
#3358=EDGE_CURVE('',#2758,#2756,#1743,.T.);
#3359=EDGE_CURVE('',#2759,#2757,#1744,.T.);
#3360=EDGE_CURVE('',#2759,#2760,#1745,.T.);
#3361=EDGE_CURVE('',#2760,#2758,#1746,.T.);
#3362=EDGE_CURVE('',#2761,#2759,#1747,.T.);
#3363=EDGE_CURVE('',#2761,#2762,#1748,.T.);
#3364=EDGE_CURVE('',#2762,#2760,#1749,.T.);
#3365=EDGE_CURVE('',#2752,#2761,#1750,.T.);
#3366=EDGE_CURVE('',#2754,#2762,#1751,.T.);
#3367=EDGE_CURVE('',#2763,#2763,#2343,.T.);
#3368=EDGE_CURVE('',#2764,#2764,#2344,.T.);
#3369=EDGE_CURVE('',#2764,#2763,#1752,.T.);
#3370=EDGE_CURVE('',#2765,#2765,#2345,.F.);
#3371=EDGE_CURVE('',#2765,#2764,#1753,.T.);
#3372=EDGE_CURVE('',#2766,#2766,#2346,.T.);
#3373=EDGE_CURVE('',#2766,#2765,#1754,.T.);
#4463=ORIENTED_EDGE('',*,*,#3349,.F.);
#4464=ORIENTED_EDGE('',*,*,#3350,.T.);
#4465=ORIENTED_EDGE('',*,*,#3351,.T.);
#4466=ORIENTED_EDGE('',*,*,#3352,.F.);
#4467=ORIENTED_EDGE('',*,*,#3353,.F.);
#4468=ORIENTED_EDGE('',*,*,#3354,.T.);
#4469=ORIENTED_EDGE('',*,*,#3355,.T.);
#4470=ORIENTED_EDGE('',*,*,#3350,.F.);
#4471=ORIENTED_EDGE('',*,*,#3356,.F.);
#4472=ORIENTED_EDGE('',*,*,#3357,.T.);
#4473=ORIENTED_EDGE('',*,*,#3358,.T.);
#4474=ORIENTED_EDGE('',*,*,#3354,.F.);
#4475=ORIENTED_EDGE('',*,*,#3359,.F.);
#4476=ORIENTED_EDGE('',*,*,#3360,.T.);
#4477=ORIENTED_EDGE('',*,*,#3361,.T.);
#4478=ORIENTED_EDGE('',*,*,#3357,.F.);
#4479=ORIENTED_EDGE('',*,*,#3362,.F.);
#4480=ORIENTED_EDGE('',*,*,#3363,.T.);
#4481=ORIENTED_EDGE('',*,*,#3364,.T.);
#4482=ORIENTED_EDGE('',*,*,#3360,.F.);
#4483=ORIENTED_EDGE('',*,*,#3365,.F.);
#4484=ORIENTED_EDGE('',*,*,#3352,.T.);
#4485=ORIENTED_EDGE('',*,*,#3366,.T.);
#4486=ORIENTED_EDGE('',*,*,#3363,.F.);
#4487=ORIENTED_EDGE('',*,*,#3366,.F.);
#4488=ORIENTED_EDGE('',*,*,#3351,.F.);
#4489=ORIENTED_EDGE('',*,*,#3355,.F.);
#4490=ORIENTED_EDGE('',*,*,#3358,.F.);
#4491=ORIENTED_EDGE('',*,*,#3361,.F.);
#4492=ORIENTED_EDGE('',*,*,#3364,.F.);
#4493=ORIENTED_EDGE('',*,*,#3367,.F.);
#4494=ORIENTED_EDGE('',*,*,#3349,.T.);
#4495=ORIENTED_EDGE('',*,*,#3365,.T.);
#4496=ORIENTED_EDGE('',*,*,#3362,.T.);
#4497=ORIENTED_EDGE('',*,*,#3359,.T.);
#4498=ORIENTED_EDGE('',*,*,#3356,.T.);
#4499=ORIENTED_EDGE('',*,*,#3353,.T.);
#4500=ORIENTED_EDGE('',*,*,#3368,.F.);
#4501=ORIENTED_EDGE('',*,*,#3369,.T.);
#4502=ORIENTED_EDGE('',*,*,#3367,.T.);
#4503=ORIENTED_EDGE('',*,*,#3369,.F.);
#4504=ORIENTED_EDGE('',*,*,#3370,.F.);
#4505=ORIENTED_EDGE('',*,*,#3371,.T.);
#4506=ORIENTED_EDGE('',*,*,#3368,.T.);
#4507=ORIENTED_EDGE('',*,*,#3371,.F.);
#4508=ORIENTED_EDGE('',*,*,#3372,.F.);
#4509=ORIENTED_EDGE('',*,*,#3373,.T.);
#4510=ORIENTED_EDGE('',*,*,#3370,.T.);
#4511=ORIENTED_EDGE('',*,*,#3373,.F.);
#4512=ORIENTED_EDGE('',*,*,#3372,.T.);
#4953=CYLINDRICAL_SURFACE('',#6163,0.24505);
#5188=ADVANCED_FACE('',(#976),#710,.F.);
#5189=ADVANCED_FACE('',(#977),#711,.F.);
#5190=ADVANCED_FACE('',(#978),#712,.F.);
#5191=ADVANCED_FACE('',(#979),#713,.F.);
#5192=ADVANCED_FACE('',(#980),#714,.F.);
#5193=ADVANCED_FACE('',(#981),#715,.F.);
#5194=ADVANCED_FACE('',(#982),#716,.F.);
#5195=ADVANCED_FACE('',(#983,#581),#717,.T.);
#5196=ADVANCED_FACE('',(#984),#312,.T.);
#5197=ADVANCED_FACE('',(#985),#4953,.T.);
#5198=ADVANCED_FACE('',(#986),#313,.T.);
#5199=ADVANCED_FACE('',(#987),#718,.T.);
#5324=CLOSED_SHELL('',(#5188,#5189,#5190,#5191,#5192,#5193,#5194,#5195,
#5196,#5197,#5198,#5199));
#6151=AXIS2_PLACEMENT_3D('',#9575,#7548,#7549);
#6152=AXIS2_PLACEMENT_3D('',#9576,#7550,#7551);
#6153=AXIS2_PLACEMENT_3D('',#9585,#7556,#7557);
#6154=AXIS2_PLACEMENT_3D('',#9591,#7561,#7562);
#6155=AXIS2_PLACEMENT_3D('',#9597,#7566,#7567);
#6156=AXIS2_PLACEMENT_3D('',#9603,#7571,#7572);
#6157=AXIS2_PLACEMENT_3D('',#9609,#7576,#7577);
#6158=AXIS2_PLACEMENT_3D('',#9612,#7580,#7581);
#6159=AXIS2_PLACEMENT_3D('',#9613,#7582,#7583);
#6160=AXIS2_PLACEMENT_3D('',#9615,#7584,#7585);
#6161=AXIS2_PLACEMENT_3D('',#9616,#7586,#7587);
#6162=AXIS2_PLACEMENT_3D('',#9618,#7588,#7589);
#6163=AXIS2_PLACEMENT_3D('',#9620,#7591,#7592);
#6164=AXIS2_PLACEMENT_3D('',#9622,#7593,#7594);
#6165=AXIS2_PLACEMENT_3D('',#9624,#7596,#7597);
#6166=AXIS2_PLACEMENT_3D('',#9626,#7598,#7599);
#6167=AXIS2_PLACEMENT_3D('',#9628,#7601,#7602);
#7548=DIRECTION('axis',(0.,0.,1.));
#7549=DIRECTION('refdir',(1.,0.,0.));
#7550=DIRECTION('center_axis',(0.866025403784439,0.,-0.5));
#7551=DIRECTION('ref_axis',(0.5,0.,0.866025403784439));
#7552=DIRECTION('',(0.5,0.,0.866025403784439));
#7553=DIRECTION('',(0.,-1.,0.));
#7554=DIRECTION('',(0.5,0.,0.866025403784439));
#7555=DIRECTION('',(0.,-1.,0.));
#7556=DIRECTION('center_axis',(1.92296268638356E-16,0.,-1.));
#7557=DIRECTION('ref_axis',(1.,0.,1.92296268638356E-16));
#7558=DIRECTION('',(1.,0.,1.92296268638356E-16));
#7559=DIRECTION('',(0.,-1.,0.));
#7560=DIRECTION('',(1.,0.,1.92296268638356E-16));
#7561=DIRECTION('center_axis',(-0.866025403784439,0.,-0.5));
#7562=DIRECTION('ref_axis',(0.5,0.,-0.866025403784439));
#7563=DIRECTION('',(0.5,0.,-0.866025403784439));
#7564=DIRECTION('',(0.,-1.,0.));
#7565=DIRECTION('',(0.5,0.,-0.866025403784438));
#7566=DIRECTION('center_axis',(-0.866025403784439,0.,0.5));
#7567=DIRECTION('ref_axis',(-0.5,0.,-0.866025403784439));
#7568=DIRECTION('',(-0.5,0.,-0.866025403784439));
#7569=DIRECTION('',(0.,-1.,0.));
#7570=DIRECTION('',(-0.5,0.,-0.866025403784439));
#7571=DIRECTION('center_axis',(-1.92296268638356E-16,0.,1.));
#7572=DIRECTION('ref_axis',(-1.,0.,-1.92296268638356E-16));
#7573=DIRECTION('',(-1.,0.,-1.92296268638356E-16));
#7574=DIRECTION('',(0.,-1.,0.));
#7575=DIRECTION('',(-1.,0.,-1.92296268638356E-16));
#7576=DIRECTION('center_axis',(0.866025403784439,0.,0.5));
#7577=DIRECTION('ref_axis',(-0.5,0.,0.866025403784439));
#7578=DIRECTION('',(-0.5,0.,0.866025403784439));
#7579=DIRECTION('',(-0.5,0.,0.866025403784439));
#7580=DIRECTION('center_axis',(0.,-1.,0.));
#7581=DIRECTION('ref_axis',(0.,0.,-1.));
#7582=DIRECTION('center_axis',(0.,1.,0.));
#7583=DIRECTION('ref_axis',(0.,0.,1.));
#7584=DIRECTION('center_axis',(0.,-1.,0.));
#7585=DIRECTION('ref_axis',(1.,0.,0.));
#7586=DIRECTION('center_axis',(0.,-1.,0.));
#7587=DIRECTION('ref_axis',(1.,0.,0.));
#7588=DIRECTION('center_axis',(0.,-1.,0.));
#7589=DIRECTION('ref_axis',(1.,0.,0.));
#7590=DIRECTION('',(0.707106781186547,0.707106781186548,8.65956056235493E-17));
#7591=DIRECTION('center_axis',(0.,-1.,0.));
#7592=DIRECTION('ref_axis',(1.,0.,0.));
#7593=DIRECTION('center_axis',(0.,1.,0.));
#7594=DIRECTION('ref_axis',(1.,0.,0.));
#7595=DIRECTION('',(0.,1.,0.));
#7596=DIRECTION('center_axis',(0.,1.,0.));
#7597=DIRECTION('ref_axis',(1.,0.,0.));
#7598=DIRECTION('center_axis',(0.,-1.,0.));
#7599=DIRECTION('ref_axis',(1.,0.,0.));
#7600=DIRECTION('',(-0.707106781186547,0.707106781186548,-8.65956056235493E-17));
#7601=DIRECTION('center_axis',(0.,-1.,0.));
#7602=DIRECTION('ref_axis',(0.,0.,-1.));
#9575=CARTESIAN_POINT('',(0.,0.,0.));
#9576=CARTESIAN_POINT('Origin',(0.0721687836487032,0.,-0.125));
#9577=CARTESIAN_POINT('',(0.0721687836487032,0.,-0.125));
#9578=CARTESIAN_POINT('',(0.144337567297406,0.,0.));
#9579=CARTESIAN_POINT('',(0.117710979560879,0.,-0.0461186027918559));
#9580=CARTESIAN_POINT('',(0.0721687836487032,-0.25,-0.125));
#9581=CARTESIAN_POINT('',(0.0721687836487032,0.,-0.125));
#9582=CARTESIAN_POINT('',(0.144337567297406,-0.25,0.));
#9583=CARTESIAN_POINT('',(0.144337567297406,-0.25,0.));
#9584=CARTESIAN_POINT('',(0.144337567297406,0.,0.));
#9585=CARTESIAN_POINT('Origin',(-0.0721687836487032,0.,-0.125));
#9586=CARTESIAN_POINT('',(-0.0721687836487032,0.,-0.125));
#9587=CARTESIAN_POINT('',(0.0739156081756484,0.,-0.125));
#9588=CARTESIAN_POINT('',(-0.0721687836487032,-0.25,-0.125));
#9589=CARTESIAN_POINT('',(-0.0721687836487032,0.,-0.125));
#9590=CARTESIAN_POINT('',(0.0721687836487032,-0.25,-0.125));
#9591=CARTESIAN_POINT('Origin',(-0.144337567297406,0.,-4.16333634234434E-17));
#9592=CARTESIAN_POINT('',(-0.144337567297406,0.,-1.76762539787485E-17));
#9593=CARTESIAN_POINT('',(-0.0987953713852306,0.,-0.0788813972081442));
#9594=CARTESIAN_POINT('',(-0.144337567297406,-0.25,-2.77555756156289E-17));
#9595=CARTESIAN_POINT('',(-0.144337567297406,0.,-1.76762539787485E-17));
#9596=CARTESIAN_POINT('',(-0.0721687836487032,-0.25,-0.125));
#9597=CARTESIAN_POINT('Origin',(-0.0721687836487033,0.,0.125));
#9598=CARTESIAN_POINT('',(-0.0721687836487033,0.,0.125));
#9599=CARTESIAN_POINT('',(-0.0627109795608791,0.,0.141381397208144));
#9600=CARTESIAN_POINT('',(-0.0721687836487033,-0.25,0.125));
#9601=CARTESIAN_POINT('',(-0.0721687836487033,0.,0.125));
#9602=CARTESIAN_POINT('',(-0.144337567297406,-0.25,-1.76762539787485E-17));
#9603=CARTESIAN_POINT('Origin',(0.0721687836487032,0.,0.125));
#9604=CARTESIAN_POINT('',(0.0721687836487032,0.,0.125));
#9605=CARTESIAN_POINT('',(0.146084391824352,0.,0.125));
#9606=CARTESIAN_POINT('',(0.0721687836487032,-0.25,0.125));
#9607=CARTESIAN_POINT('',(0.0721687836487032,0.,0.125));
#9608=CARTESIAN_POINT('',(-0.0721687836487033,-0.25,0.125));
#9609=CARTESIAN_POINT('Origin',(0.144337567297406,0.,0.));
#9610=CARTESIAN_POINT('',(0.153795371385231,0.,-0.0163813972081441));
#9611=CARTESIAN_POINT('',(0.0721687836487032,-0.25,0.125));
#9612=CARTESIAN_POINT('Origin',(0.,-0.25,0.));
#9613=CARTESIAN_POINT('Origin',(0.22,0.,0.));
#9614=CARTESIAN_POINT('',(-0.22,-8.67361737988404E-18,-2.69422295812418E-17));
#9615=CARTESIAN_POINT('Origin',(0.,0.,0.));
#9616=CARTESIAN_POINT('Origin',(0.,-0.015,0.));
#9617=CARTESIAN_POINT('',(-0.24505,-0.02505,-3.00099698131059E-17));
#9618=CARTESIAN_POINT('Origin',(0.,-0.02505,0.));
#9619=CARTESIAN_POINT('',(-0.235,-0.015,-2.87791997799628E-17));
#9620=CARTESIAN_POINT('Origin',(0.,-0.3775,0.));
#9621=CARTESIAN_POINT('',(-0.24505,-0.72995,3.00099698131059E-17));
#9622=CARTESIAN_POINT('Origin',(0.,-0.72995,0.));
#9623=CARTESIAN_POINT('',(-0.24505,-0.3775,-3.00099698131059E-17));
#9624=CARTESIAN_POINT('Origin',(0.,-0.7625,0.));
#9625=CARTESIAN_POINT('',(-0.175,-0.8,-2.14313189850787E-17));
#9626=CARTESIAN_POINT('Origin',(0.,-0.8,0.));
#9627=CARTESIAN_POINT('',(-0.2125,-0.7625,-2.60237444818813E-17));
#9628=CARTESIAN_POINT('Origin',(0.,-0.8,0.));
#10459=UNCERTAINTY_MEASURE_WITH_UNIT(LENGTH_MEASURE(0.001),#10511,
'DISTANCE_ACCURACY_VALUE',
'Maximum model space distance between geometric entities at asserted c
onnectivities');
#10471=UNCERTAINTY_MEASURE_WITH_UNIT(LENGTH_MEASURE(0.001),#10511,
'DISTANCE_ACCURACY_VALUE',
'Maximum model space distance between geometric entities at asserted c
onnectivities');
#10498=(
GEOMETRIC_REPRESENTATION_CONTEXT(3)
GLOBAL_UNCERTAINTY_ASSIGNED_CONTEXT((#10459))
GLOBAL_UNIT_ASSIGNED_CONTEXT((#10511,#10513,#10514))
REPRESENTATION_CONTEXT('','3D')
);
#10510=(
GEOMETRIC_REPRESENTATION_CONTEXT(3)
GLOBAL_UNCERTAINTY_ASSIGNED_CONTEXT((#10471))
GLOBAL_UNIT_ASSIGNED_CONTEXT((#10511,#10513,#10514))
REPRESENTATION_CONTEXT('','3D')
);
#10511=(
LENGTH_UNIT()
NAMED_UNIT(*)
SI_UNIT(.CENTI.,.METRE.)
);
#10513=(
NAMED_UNIT(*)
PLANE_ANGLE_UNIT()
SI_UNIT($,.RADIAN.)
);
#10514=(
NAMED_UNIT(*)
SI_UNIT($,.STERADIAN.)
SOLID_ANGLE_UNIT()
);
#10541=SHAPE_DEFINITION_REPRESENTATION(#10584,#10671);
#10584=PRODUCT_DEFINITION_SHAPE('',$,#10710);
#10671=SHAPE_REPRESENTATION('',(#6151),#10498);
#10683=PRODUCT_DEFINITION_CONTEXT('part definition',#10799,'design');
#10710=PRODUCT_DEFINITION('Socket Set Screw - M5x8',
'Socket Set Screw - M5x8',#10748,#10683);
#10748=PRODUCT_DEFINITION_FORMATION('',$,#10827);
#10799=APPLICATION_CONTEXT(
'Core Data for Automotive Mechanical Design Process');
#10800=PRODUCT_CONTEXT('part definition',#10799,'mechanical');
#10827=PRODUCT('Socket Set Screw - M5x8','Socket Set Screw - M5x8',
'Socket Set Screw - M5x8',(#10800));
#10909=COLOUR_RGB('Black',0.12,0.14,0.17);
#10910=FILL_AREA_STYLE_COLOUR('',#10909);
#10911=FILL_AREA_STYLE('',(#10910));
#10912=SURFACE_STYLE_FILL_AREA(#10911);
#10913=SURFACE_SIDE_STYLE('',(#10912));
#10914=SURFACE_STYLE_USAGE(.BOTH.,#10913);
#10915=PRESENTATION_STYLE_ASSIGNMENT((#10914));
ENDSEC;
END-ISO-10303-21;
